ISO-10303-21;
HEADER;
FILE_DESCRIPTION (('STEP AP214'),
    '1' );
FILE_NAME ('din_6885_2_a_6_x_6_x_25.step',
    '2026-11-01T05:08:46',
    ( '' ),
    ( '' ),
    'SwSTEP 2.0',
    'SolidWorks 2024',
    '' );
FILE_SCHEMA (( 'AUTOMOTIVE_DESIGN' ));
ENDSEC;

DATA;
#51=PRODUCT_DEFINITION_CONTEXT ( 'detailed design', #7403, 'design' ) ;
#89=AXIS2_PLACEMENT_3D ( 'NONE', #16436, #15148, #1397 ) ;
#197=VERTEX_POINT ( 'NONE', #10901 ) ;
#219=VERTEX_POINT ( 'NONE', #3420 ) ;
#347=ORIENTED_EDGE ( 'NONE', *, *, #12525, .F. ) ;
#459=ORIENTED_EDGE ( 'NONE', *, *, #16113, .T. ) ;
#573=CARTESIAN_POINT ( 'NONE',  ( 3.000000000000000000, 1.836909530733565148E-16, 22.00000000000000000 ) ) ;
#753=SURFACE_SIDE_STYLE ('',( #5726 ) ) ;
#792=DIRECTION ( 'NONE',  ( -6.123031769111888756E-17, 0.000000000000000000, -1.000000000000000000 ) ) ;
#1126=LINE ( 'NONE', #10572, #5684 ) ;
#1211=FACE_OUTER_BOUND ( 'NONE', #7622, .T. ) ;
#1247=ORIENTED_EDGE ( 'NONE', *, *, #8989, .T. ) ;
#1355=AXIS2_PLACEMENT_3D ( 'NONE', #12281, #16142, #12107 ) ;
#1397=DIRECTION ( 'NONE',  ( 7.900838015626929923E-17, 8.586860021784410058E-33, -1.000000000000000000 ) ) ;
#1423=CARTESIAN_POINT ( 'NONE',  ( 1.209468180989048008E-15, 2.719172340231729715E-32, 12.50000000000000000 ) ) ;
#1488=AXIS2_PLACEMENT_3D ( 'NONE', #3280, #8693, #15217 ) ;
#1775=AXIS2_PLACEMENT_3D ( 'NONE', #7876, #4957, #5131 ) ;
#1808=PRODUCT_DEFINITION ( 'UNKNOWN', '', #5601, #51 ) ;
#1831=CYLINDRICAL_SURFACE ( 'NONE', #16503, 2.999999999999999112 ) ;
#1876=LINE ( 'NONE', #16548, #14994 ) ;
#1934=LINE ( 'NONE', #573, #6396 ) ;
#1976=AXIS2_PLACEMENT_3D ( 'NONE', #7527, #16886, #13122 ) ;
#2017=LINE ( 'NONE', #12333, #11515 ) ;
#2076=VECTOR ( 'NONE', #10731, 1000.000000000000000 ) ;
#2087=ORIENTED_EDGE ( 'NONE', *, *, #13927, .T. ) ;
#2232=CARTESIAN_POINT ( 'NONE',  ( -3.000000000000000000, -1.836909530733565148E-16, 3.000000000000000000 ) ) ;
#2290=CIRCLE ( 'NONE', #4227, 2.999999999999999112 ) ;
#2374=DIRECTION ( 'NONE',  ( -7.900838015626929923E-17, -8.586860021784410058E-33, 1.000000000000000000 ) ) ;
#2400=SHAPE_REPRESENTATION_RELATIONSHIP ( 'NONE' , 'NONE' ,  #8805, #10584 ) ;
#2443=PRODUCT ( 'din_6885_2_a_6_x_6_x_25', 'din_6885_2_a_6_x_6_x_25', '', ( #11008 ) ) ;
#2491=ORIENTED_EDGE ( 'NONE', *, *, #5705, .T. ) ;
#2553=CARTESIAN_POINT ( 'NONE',  ( 9.796850830579020038E-16, 6.000000000000000000, 22.00000000000000000 ) ) ;
#2587=DIRECTION ( 'NONE',  ( -6.123031769111888756E-17, 1.000000000000000000, 3.749151804555344967E-33 ) ) ;
#2607=CARTESIAN_POINT ( 'NONE',  ( 1.347066989204613998E-15, 0.000000000000000000, 22.00000000000000000 ) ) ;
#2681=CARTESIAN_POINT ( 'NONE',  ( 3.000000000000000000, 1.836909530733565148E-16, 22.00000000000000000 ) ) ;
#2696=EDGE_CURVE ( 'NONE', #12703, #9577, #3660, .T. ) ;
#2836=LINE ( 'NONE', #16148, #2076 ) ;
#2928=CARTESIAN_POINT ( 'NONE',  ( 1.347066989204613998E-15, 6.000000000000000000, 24.99999999999999645 ) ) ;
#3008=CARTESIAN_POINT ( 'NONE',  ( -3.000000000000000000, -1.836909530733565148E-16, 12.50000000000000000 ) ) ;
#3270=VERTEX_POINT ( 'NONE', #15954 ) ;
#3280=CARTESIAN_POINT ( 'NONE',  ( 0.000000000000000000, 0.000000000000000000, 0.000000000000000000 ) ) ;
#3408=( NAMED_UNIT ( * ) SI_UNIT ( $, .STERADIAN. ) SOLID_ANGLE_UNIT ( ) );
#3420=CARTESIAN_POINT ( 'NONE',  ( 3.000000000000000000, 1.836909530733565148E-16, 22.00000000000000000 ) ) ;
#3560=EDGE_CURVE ( 'NONE', #5152, #4052, #4785, .T. ) ;
#3617=LINE ( 'NONE', #2232, #7234 ) ;
#3660=CIRCLE ( 'NONE', #14903, 3.000000000000000000 ) ;
#3843=EDGE_CURVE ( 'NONE', #219, #4052, #1934, .T. ) ;
#3956=( NAMED_UNIT ( * ) SI_UNIT ( $, .STERADIAN. ) SOLID_ANGLE_UNIT ( ) );
#4046=ORIENTED_EDGE ( 'NONE', *, *, #3560, .F. ) ;
#4052=VERTEX_POINT ( 'NONE', #10239 ) ;
#4227=AXIS2_PLACEMENT_3D ( 'NONE', #2607, #15403, #12829 ) ;
#4258=ORIENTED_EDGE ( 'NONE', *, *, #10449, .T. ) ;
#4292=ORIENTED_EDGE ( 'NONE', *, *, #13510, .F. ) ;
#4308=PLANE ( 'NONE',  #15751 ) ;
#4407=DIRECTION ( 'NONE',  ( 6.123031769111888756E-17, -1.000000000000000000, -3.749151804555344967E-33 ) ) ;
#4567=AXIS2_PLACEMENT_3D ( 'NONE', #14165, #15447, #6318 ) ;
#4681=ORIENTED_EDGE ( 'NONE', *, *, #16934, .F. ) ;
#4785=LINE ( 'NONE', #7351, #5453 ) ;
#4957=DIRECTION ( 'NONE',  ( -6.123031769111888756E-17, 1.000000000000000000, 3.749151804555344967E-33 ) ) ;
#5131=DIRECTION ( 'NONE',  ( 6.123031769111888756E-17, 0.000000000000000000, 1.000000000000000000 ) ) ;
#5152=VERTEX_POINT ( 'NONE', #9776 ) ;
#5453=VECTOR ( 'NONE', #2374, 1000.000000000000000 ) ;
#5512=DIRECTION ( 'NONE',  ( 6.123031769111888756E-17, 0.000000000000000000, 1.000000000000000000 ) ) ;
#5601=PRODUCT_DEFINITION_FORMATION_WITH_SPECIFIED_SOURCE ( 'ANY', '', #2443, .NOT_KNOWN. ) ;
#5609=CARTESIAN_POINT ( 'NONE',  ( 1.836909530733565148E-16, 0.000000000000000000, 3.000000000000000000 ) ) ;
#5619=VERTEX_POINT ( 'NONE', #2928 ) ;
#5664=APPLICATION_CONTEXT ( 'automotive_design' ) ;
#5684=VECTOR ( 'NONE', #2587, 1000.000000000000000 ) ;
#5705=EDGE_CURVE ( 'NONE', #5619, #5778, #2836, .T. ) ;
#5726=SURFACE_STYLE_FILL_AREA ( #11136 ) ;
#5778=VERTEX_POINT ( 'NONE', #11239 ) ;
#5916=EDGE_CURVE ( 'NONE', #197, #5152, #9505, .T. ) ;
#5974=FILL_AREA_STYLE_COLOUR ( '', #13761 ) ;
#6056=DIRECTION ( 'NONE',  ( -1.000000000000000000, -6.123031769111888756E-17, 6.123031769111888756E-17 ) ) ;
#6086=ORIENTED_EDGE ( 'NONE', *, *, #2696, .T. ) ;
#6220=FACE_OUTER_BOUND ( 'NONE', #6255, .T. ) ;
#6255=EDGE_LOOP ( 'NONE', ( #12063, #11659, #459, #12207 ) ) ;
#6257=CARTESIAN_POINT ( 'NONE',  ( 1.347066989204613998E-15, 0.000000000000000000, 22.00000000000000000 ) ) ;
#6318=DIRECTION ( 'NONE',  ( 6.123031769111888756E-17, 0.000000000000000000, 1.000000000000000000 ) ) ;
#6396=VECTOR ( 'NONE', #15002, 1000.000000000000000 ) ;
#6612=( GEOMETRIC_REPRESENTATION_CONTEXT ( 3 ) GLOBAL_UNCERTAINTY_ASSIGNED_CONTEXT ( ( #15342 ) ) GLOBAL_UNIT_ASSIGNED_CONTEXT ( ( #15168, #13795, #3408 ) ) REPRESENTATION_CONTEXT ( 'NONE', 'WORKASPACE' ) );
#6643=DIRECTION ( 'NONE',  ( -6.123031769111888756E-17, 1.000000000000000000, 3.749151804555346336E-33 ) ) ;
#6816=EDGE_CURVE ( 'NONE', #12703, #5152, #1126, .T. ) ;
#7013=EDGE_LOOP ( 'NONE', ( #9535, #12114, #6086, #1247 ) ) ;
#7099=AXIS2_PLACEMENT_3D ( 'NONE', #1423, #6643, #10696 ) ;
#7234=VECTOR ( 'NONE', #11682, 1000.000000000000000 ) ;
#7299=LINE ( 'NONE', #12549, #7377 ) ;
#7351=CARTESIAN_POINT ( 'NONE',  ( 3.000000000000000000, 6.000000000000000000, 22.00000000000000000 ) ) ;
#7377=VECTOR ( 'NONE', #792, 1000.000000000000000 ) ;
#7381=CYLINDRICAL_SURFACE ( 'NONE', #13015, 2.999999999999999112 ) ;
#7403=APPLICATION_CONTEXT ( 'automotive_design' ) ;
#7486=EDGE_CURVE ( 'NONE', #15703, #3270, #1876, .T. ) ;
#7527=CARTESIAN_POINT ( 'NONE',  ( 9.796850830579020038E-16, 6.000000000000000000, 22.00000000000000000 ) ) ;
#7572=FACE_OUTER_BOUND ( 'NONE', #11190, .T. ) ;
#7622=EDGE_LOOP ( 'NONE', ( #11893, #2491, #9308, #8780 ) ) ;
#7649=LINE ( 'NONE', #2681, #10465 ) ;
#7714=DIRECTION ( 'NONE',  ( 6.123031769111888756E-17, -1.000000000000000000, -3.749151804555344967E-33 ) ) ;
#7876=CARTESIAN_POINT ( 'NONE',  ( 1.347066989204613998E-15, 0.000000000000000000, 22.00000000000000000 ) ) ;
#7909=DIRECTION ( 'NONE',  ( 7.900838015626929923E-17, 8.586860021784410058E-33, -1.000000000000000000 ) ) ;
#8261=DIRECTION ( 'NONE',  ( 6.123031769111888756E-17, 0.000000000000000000, 1.000000000000000000 ) ) ;
#8325=PLANE ( 'NONE',  #1355 ) ;
#8693=DIRECTION ( 'NONE',  ( 0.000000000000000000, 0.000000000000000000, 1.000000000000000000 ) ) ;
#8780=ORIENTED_EDGE ( 'NONE', *, *, #3843, .T. ) ;
#8805=SHAPE_REPRESENTATION ( 'din_6885_2_a_6_x_6_x_25', ( #1488 ), #16299 ) ;
#8926=DIRECTION ( 'NONE',  ( 6.123031769111888756E-17, -1.000000000000000000, -3.749151804555344967E-33 ) ) ;
#8989=EDGE_CURVE ( 'NONE', #9577, #197, #2017, .T. ) ;
#9172=CIRCLE ( 'NONE', #1775, 2.999999999999999112 ) ;
#9308=ORIENTED_EDGE ( 'NONE', *, *, #12525, .T. ) ;
#9504=PLANE ( 'NONE',  #7099 ) ;
#9505=CIRCLE ( 'NONE', #4567, 3.000000000000000000 ) ;
#9535=ORIENTED_EDGE ( 'NONE', *, *, #5916, .T. ) ;
#9577=VERTEX_POINT ( 'NONE', #16663 ) ;
#9648=CARTESIAN_POINT ( 'NONE',  ( 1.347066989204613998E-15, 0.000000000000000000, 22.00000000000000000 ) ) ;
#9687=AXIS2_PLACEMENT_3D ( 'NONE', #2553, #8926, #14164 ) ;
#9776=CARTESIAN_POINT ( 'NONE',  ( 3.000000000000000000, 6.000000000000000000, 3.000000000000000000 ) ) ;
#9867=ORIENTED_EDGE ( 'NONE', *, *, #11193, .F. ) ;
#9915=PLANE ( 'NONE',  #89 ) ;
#10204=CIRCLE ( 'NONE', #1976, 2.999999999999999112 ) ;
#10239=CARTESIAN_POINT ( 'NONE',  ( 3.000000000000000000, 6.000000000000000000, 22.00000000000000000 ) ) ;
#10394=EDGE_LOOP ( 'NONE', ( #14504, #13109, #11964, #347, #4681 ) ) ;
#10449=EDGE_CURVE ( 'NONE', #219, #12703, #7649, .T. ) ;
#10465=VECTOR ( 'NONE', #7909, 1000.000000000000000 ) ;
#10487=ADVANCED_FACE ( 'NONE', ( #14801 ), #1831, .T. ) ;
#10572=CARTESIAN_POINT ( 'NONE',  ( 3.000000000000000000, 1.836909530733570325E-16, 3.000000000000000000 ) ) ;
#10583=EDGE_LOOP ( 'NONE', ( #13734, #2087, #16689, #15407 ) ) ;
#10584=ADVANCED_BREP_SHAPE_REPRESENTATION ( '', ( #14050, #1488 ), #16299 ) ;
#10696=DIRECTION ( 'NONE',  ( 6.123031769111888756E-17, 0.000000000000000000, 1.000000000000000000 ) ) ;
#10731=DIRECTION ( 'NONE',  ( 6.123031769111888756E-17, -1.000000000000000000, -3.749151804555344967E-33 ) ) ;
#10901=CARTESIAN_POINT ( 'NONE',  ( -3.000000000000000000, 6.000000000000000000, 3.000000000000000000 ) ) ;
#10909=FACE_OUTER_BOUND ( 'NONE', #12542, .T. ) ;
#10967=SURFACE_STYLE_USAGE ( .BOTH. , #753 ) ;
#11008=PRODUCT_CONTEXT ( 'NONE', #5664, 'mechanical' ) ;
#11036=CARTESIAN_POINT ( 'NONE',  ( 1.836909530733565148E-16, 0.000000000000000000, 3.000000000000000000 ) ) ;
#11136=FILL_AREA_STYLE ('',( #5974 ) ) ;
#11190=EDGE_LOOP ( 'NONE', ( #14357, #14969, #4258, #16918 ) ) ;
#11193=EDGE_CURVE ( 'NONE', #4052, #5619, #15162, .T. ) ;
#11204=CYLINDRICAL_SURFACE ( 'NONE', #11800, 3.000000000000000000 ) ;
#11239=CARTESIAN_POINT ( 'NONE',  ( 1.347066989204613998E-15, -1.203706215242022682E-32, 24.99999999999999645 ) ) ;
#11251=SHAPE_DEFINITION_REPRESENTATION ( #13611, #8805 ) ;
#11397=DIRECTION ( 'NONE',  ( -6.123031769111888756E-17, 1.000000000000000000, 3.749151804555344967E-33 ) ) ;
#11505=( LENGTH_UNIT ( ) NAMED_UNIT ( * ) SI_UNIT ( .MILLI., .METRE. ) );
#11508=DIRECTION ( 'NONE',  ( 6.123031769111888756E-17, 0.000000000000000000, 1.000000000000000000 ) ) ;
#11515=VECTOR ( 'NONE', #16286, 1000.000000000000000 ) ;
#11583=ADVANCED_FACE ( 'NONE', ( #7572 ), #9915, .T. ) ;
#11659=ORIENTED_EDGE ( 'NONE', *, *, #8989, .F. ) ;
#11682=DIRECTION ( 'NONE',  ( 6.123031769111888756E-17, 0.000000000000000000, 1.000000000000000000 ) ) ;
#11800=AXIS2_PLACEMENT_3D ( 'NONE', #11036, #13869, #16361 ) ;
#11893=ORIENTED_EDGE ( 'NONE', *, *, #11193, .T. ) ;
#11964=ORIENTED_EDGE ( 'NONE', *, *, #10449, .F. ) ;
#12063=ORIENTED_EDGE ( 'NONE', *, *, #13510, .T. ) ;
#12107=DIRECTION ( 'NONE',  ( 6.123031769111888756E-17, 0.000000000000000000, 1.000000000000000000 ) ) ;
#12114=ORIENTED_EDGE ( 'NONE', *, *, #6816, .F. ) ;
#12207=ORIENTED_EDGE ( 'NONE', *, *, #7486, .T. ) ;
#12281=CARTESIAN_POINT ( 'NONE',  ( 8.420862748423350279E-16, 6.000000000000000000, 12.50000000000000000 ) ) ;
#12333=CARTESIAN_POINT ( 'NONE',  ( -3.000000000000000000, -1.836909530733565148E-16, 3.000000000000000000 ) ) ;
#12525=EDGE_CURVE ( 'NONE', #5778, #219, #9172, .T. ) ;
#12542=EDGE_LOOP ( 'NONE', ( #15414, #4292, #15547, #9867, #4046 ) ) ;
#12549=CARTESIAN_POINT ( 'NONE',  ( -3.000000000000000000, 6.000000000000000000, 3.000000000000000000 ) ) ;
#12703=VERTEX_POINT ( 'NONE', #15784 ) ;
#12829=DIRECTION ( 'NONE',  ( 6.123031769111888756E-17, 0.000000000000000000, 1.000000000000000000 ) ) ;
#12931=MECHANICAL_DESIGN_GEOMETRIC_PRESENTATION_REPRESENTATION('',(#14041),#6612);
#13015=AXIS2_PLACEMENT_3D ( 'NONE', #6257, #7714, #11508 ) ;
#13109=ORIENTED_EDGE ( 'NONE', *, *, #2696, .F. ) ;
#13122=DIRECTION ( 'NONE',  ( 6.123031769111888756E-17, 0.000000000000000000, 1.000000000000000000 ) ) ;
#13163=ADVANCED_FACE ( 'NONE', ( #13197 ), #9504, .F. ) ;
#13196=ADVANCED_FACE ( 'NONE', ( #14995 ), #11204, .T. ) ;
#13197=FACE_OUTER_BOUND ( 'NONE', #10394, .T. ) ;
#13510=EDGE_CURVE ( 'NONE', #3270, #197, #7299, .T. ) ;
#13611=PRODUCT_DEFINITION_SHAPE ( 'NONE', 'NONE',  #1808 ) ;
#13632=ADVANCED_FACE ( 'NONE', ( #10909 ), #8325, .T. ) ;
#13734=ORIENTED_EDGE ( 'NONE', *, *, #5705, .F. ) ;
#13761=COLOUR_RGB ( '', 0.09019608, 0.27058824, 0.51372549) ;
#13795=( NAMED_UNIT ( * ) PLANE_ANGLE_UNIT ( ) SI_UNIT ( $, .RADIAN. ) );
#13869=DIRECTION ( 'NONE',  ( 6.123031769111888756E-17, -1.000000000000000000, -3.749151804555344967E-33 ) ) ;
#13927=EDGE_CURVE ( 'NONE', #5619, #3270, #10204, .T. ) ;
#14041=STYLED_ITEM ( 'NONE', ( #16202 ), #14050 ) ;
#14050=MANIFOLD_SOLID_BREP ( 'Imported1', #15945 ) ;
#14164=DIRECTION ( 'NONE',  ( 6.123031769111888756E-17, 0.000000000000000000, 1.000000000000000000 ) ) ;
#14165=CARTESIAN_POINT ( 'NONE',  ( -1.836909530733565148E-16, 6.000000000000000000, 3.000000000000000000 ) ) ;
#14258=( NAMED_UNIT ( * ) PLANE_ANGLE_UNIT ( ) SI_UNIT ( $, .RADIAN. ) );
#14357=ORIENTED_EDGE ( 'NONE', *, *, #3560, .T. ) ;
#14504=ORIENTED_EDGE ( 'NONE', *, *, #16113, .F. ) ;
#14801=FACE_OUTER_BOUND ( 'NONE', #10583, .T. ) ;
#14903=AXIS2_PLACEMENT_3D ( 'NONE', #5609, #15831, #5512 ) ;
#14969=ORIENTED_EDGE ( 'NONE', *, *, #3843, .F. ) ;
#14994=VECTOR ( 'NONE', #11397, 1000.000000000000000 ) ;
#14995=FACE_OUTER_BOUND ( 'NONE', #7013, .T. ) ;
#15002=DIRECTION ( 'NONE',  ( -6.123031769111888756E-17, 1.000000000000000000, 3.749151804555344967E-33 ) ) ;
#15148=DIRECTION ( 'NONE',  ( 1.000000000000000000, 6.123031769111888756E-17, 7.900838015626929923E-17 ) ) ;
#15162=CIRCLE ( 'NONE', #9687, 2.999999999999999112 ) ;
#15168=( LENGTH_UNIT ( ) NAMED_UNIT ( * ) SI_UNIT ( .MILLI., .METRE. ) );
#15217=DIRECTION ( 'NONE',  ( 1.000000000000000000, 0.000000000000000000, 0.000000000000000000 ) ) ;
#15342=UNCERTAINTY_MEASURE_WITH_UNIT (LENGTH_MEASURE( 1.000000000000000082E-05 ), #15168, 'distance_accuracy_value', 'NONE');
#15403=DIRECTION ( 'NONE',  ( -6.123031769111888756E-17, 1.000000000000000000, 3.749151804555344967E-33 ) ) ;
#15407=ORIENTED_EDGE ( 'NONE', *, *, #16934, .T. ) ;
#15414=ORIENTED_EDGE ( 'NONE', *, *, #5916, .F. ) ;
#15447=DIRECTION ( 'NONE',  ( 6.123031769111888756E-17, -1.000000000000000000, -3.749151804555344967E-33 ) ) ;
#15547=ORIENTED_EDGE ( 'NONE', *, *, #13927, .F. ) ;
#15703=VERTEX_POINT ( 'NONE', #16929 ) ;
#15751=AXIS2_PLACEMENT_3D ( 'NONE', #3008, #6056, #16380 ) ;
#15784=CARTESIAN_POINT ( 'NONE',  ( 3.000000000000000000, 1.836909530733570325E-16, 3.000000000000000000 ) ) ;
#15831=DIRECTION ( 'NONE',  ( -6.123031769111888756E-17, 1.000000000000000000, 3.749151804555344967E-33 ) ) ;
#15945=CLOSED_SHELL ( 'NONE', ( #16013, #13163, #13632, #16406, #10487, #11583, #13196 ) ) ;
#15954=CARTESIAN_POINT ( 'NONE',  ( -3.000000000000000000, 6.000000000000000000, 22.00000000000000000 ) ) ;
#16013=ADVANCED_FACE ( 'NONE', ( #1211 ), #7381, .T. ) ;
#16113=EDGE_CURVE ( 'NONE', #9577, #15703, #3617, .T. ) ;
#16142=DIRECTION ( 'NONE',  ( -6.123031769111888756E-17, 1.000000000000000000, 3.749151804555346336E-33 ) ) ;
#16148=CARTESIAN_POINT ( 'NONE',  ( 1.530757942277970587E-15, 0.000000000000000000, 24.99999999999999645 ) ) ;
#16202=PRESENTATION_STYLE_ASSIGNMENT (( #10967 ) ) ;
#16286=DIRECTION ( 'NONE',  ( -6.123031769111888756E-17, 1.000000000000000000, 3.749151804555344967E-33 ) ) ;
#16299=( GEOMETRIC_REPRESENTATION_CONTEXT ( 3 ) GLOBAL_UNCERTAINTY_ASSIGNED_CONTEXT ( ( #16702 ) ) GLOBAL_UNIT_ASSIGNED_CONTEXT ( ( #11505, #14258, #3956 ) ) REPRESENTATION_CONTEXT ( 'NONE', 'WORKASPACE' ) );
#16361=DIRECTION ( 'NONE',  ( 6.123031769111888756E-17, 0.000000000000000000, 1.000000000000000000 ) ) ;
#16380=DIRECTION ( 'NONE',  ( 6.123031769111888756E-17, 0.000000000000000000, 1.000000000000000000 ) ) ;
#16406=ADVANCED_FACE ( 'NONE', ( #6220 ), #4308, .T. ) ;
#16436=CARTESIAN_POINT ( 'NONE',  ( 3.000000000000000000, 1.836909530733565148E-16, 12.50000000000000000 ) ) ;
#16503=AXIS2_PLACEMENT_3D ( 'NONE', #9648, #4407, #8261 ) ;
#16548=CARTESIAN_POINT ( 'NONE',  ( -3.000000000000000000, -1.836909530733565148E-16, 22.00000000000000000 ) ) ;
#16663=CARTESIAN_POINT ( 'NONE',  ( -3.000000000000000000, -1.836909530733565148E-16, 3.000000000000000000 ) ) ;
#16689=ORIENTED_EDGE ( 'NONE', *, *, #7486, .F. ) ;
#16702=UNCERTAINTY_MEASURE_WITH_UNIT (LENGTH_MEASURE( 1.000000000000000082E-05 ), #11505, 'distance_accuracy_value', 'NONE');
#16886=DIRECTION ( 'NONE',  ( 6.123031769111888756E-17, -1.000000000000000000, -3.749151804555344967E-33 ) ) ;
#16918=ORIENTED_EDGE ( 'NONE', *, *, #6816, .T. ) ;
#16929=CARTESIAN_POINT ( 'NONE',  ( -3.000000000000000000, -1.836909530733565148E-16, 22.00000000000000000 ) ) ;
#16934=EDGE_CURVE ( 'NONE', #15703, #5778, #2290, .T. ) ;
ENDSEC;
END-ISO-10303-21;
